ISO-10303-21;
HEADER;
/* Generated by software containing ST-Developer
 * from STEP Tools, Inc. (www.steptools.com) 
 */

FILE_DESCRIPTION(
/* description */ (''),
/* implementation_level */ '2;1');

FILE_NAME(
/* name */ 'Pin_03.step',
/* time_stamp */ '2026-10-04T12:17:52-07:00',
/* author */ (''),
/* organization */ (''),
/* preprocessor_version */ 'ST-DEVELOPER v20.2',
/* originating_system */ 'Autodesk Translation Framework v15.15.0.0',
/* authorisation */ '');

FILE_SCHEMA (('AUTOMOTIVE_DESIGN { 1 0 10303 214 3 1 1 }'));
ENDSEC;

DATA;
#10=MECHANICAL_DESIGN_GEOMETRIC_PRESENTATION_REPRESENTATION('',(#64),#1602);
#48=SHAPE_REPRESENTATION_RELATIONSHIP('SRR','None',#1635,#56);
#56=ADVANCED_BREP_SHAPE_REPRESENTATION('',(#72),#1595);
#64=STYLED_ITEM('',(#1684),#72);
#72=MANIFOLD_SOLID_BREP('Body1',#775);
#111=CIRCLE('',#913,2.5);
#112=CIRCLE('',#915,2.5);
#142=CYLINDRICAL_SURFACE('',#914,2.5);
#175=FACE_OUTER_BOUND('',#224,.T.);
#176=FACE_OUTER_BOUND('',#225,.T.);
#177=FACE_OUTER_BOUND('',#226,.T.);
#224=EDGE_LOOP('',(#624));
#225=EDGE_LOOP('',(#625,#626,#627,#628));
#226=EDGE_LOOP('',(#629));
#299=LINE('',#1351,#348);
#348=VECTOR('',#1101,2.5);
#397=VERTEX_POINT('',#1346);
#398=VERTEX_POINT('',#1349);
#477=EDGE_CURVE('',#397,#397,#111,.T.);
#478=EDGE_CURVE('',#398,#398,#112,.T.);
#479=EDGE_CURVE('',#398,#397,#299,.T.);
#624=ORIENTED_EDGE('',*,*,#477,.T.);
#625=ORIENTED_EDGE('',*,*,#478,.F.);
#626=ORIENTED_EDGE('',*,*,#479,.T.);
#627=ORIENTED_EDGE('',*,*,#477,.F.);
#628=ORIENTED_EDGE('',*,*,#479,.F.);
#629=ORIENTED_EDGE('',*,*,#478,.T.);
#713=PLANE('',#912);
#714=PLANE('',#916);
#747=ADVANCED_FACE('',(#175),#713,.F.);
#748=ADVANCED_FACE('',(#176),#142,.T.);
#749=ADVANCED_FACE('',(#177),#714,.T.);
#775=CLOSED_SHELL('',(#747,#748,#749));
#911=AXIS2_PLACEMENT_3D('',#1344,#1091,#1092);
#912=AXIS2_PLACEMENT_3D('',#1345,#1093,#1094);
#913=AXIS2_PLACEMENT_3D('',#1347,#1095,#1096);
#914=AXIS2_PLACEMENT_3D('',#1348,#1097,#1098);
#915=AXIS2_PLACEMENT_3D('',#1350,#1099,#1100);
#916=AXIS2_PLACEMENT_3D('',#1352,#1102,#1103);
#1091=DIRECTION('axis',(0.,0.,1.));
#1092=DIRECTION('refdir',(1.,0.,0.));
#1093=DIRECTION('center_axis',(0.,0.,1.));
#1094=DIRECTION('ref_axis',(1.,0.,0.));
#1095=DIRECTION('center_axis',(0.,0.,-1.));
#1096=DIRECTION('ref_axis',(1.,0.,0.));
#1097=DIRECTION('center_axis',(0.,0.,1.));
#1098=DIRECTION('ref_axis',(1.,0.,0.));
#1099=DIRECTION('center_axis',(0.,0.,1.));
#1100=DIRECTION('ref_axis',(1.,0.,0.));
#1101=DIRECTION('',(0.,0.,-1.));
#1102=DIRECTION('center_axis',(0.,0.,1.));
#1103=DIRECTION('ref_axis',(1.,0.,0.));
#1344=CARTESIAN_POINT('',(0.,0.,0.));
#1345=CARTESIAN_POINT('Origin',(0.,0.,-2.));
#1346=CARTESIAN_POINT('',(-2.5,-3.06161699786838E-16,-2.));
#1347=CARTESIAN_POINT('Origin',(0.,0.,-2.));
#1348=CARTESIAN_POINT('Origin',(0.,0.,0.));
#1349=CARTESIAN_POINT('',(-2.5,-3.06161699786838E-16,5.5));
#1350=CARTESIAN_POINT('Origin',(0.,0.,5.5));
#1351=CARTESIAN_POINT('',(-2.5,-3.06161699786838E-16,0.));
#1352=CARTESIAN_POINT('Origin',(0.,0.,5.5));
#1585=UNCERTAINTY_MEASURE_WITH_UNIT(LENGTH_MEASURE(0.01),#1603,
'DISTANCE_ACCURACY_VALUE',
'Maximum model space distance between geometric entities at asserted c
onnectivities');
#1592=UNCERTAINTY_MEASURE_WITH_UNIT(LENGTH_MEASURE(0.01),#1603,
'DISTANCE_ACCURACY_VALUE',
'Maximum model space distance between geometric entities at asserted c
onnectivities');
#1595=(
GEOMETRIC_REPRESENTATION_CONTEXT(3)
GLOBAL_UNCERTAINTY_ASSIGNED_CONTEXT((#1585))
GLOBAL_UNIT_ASSIGNED_CONTEXT((#1603,#1605,#1606))
REPRESENTATION_CONTEXT('','3D')
);
#1602=(
GEOMETRIC_REPRESENTATION_CONTEXT(3)
GLOBAL_UNCERTAINTY_ASSIGNED_CONTEXT((#1592))
GLOBAL_UNIT_ASSIGNED_CONTEXT((#1603,#1605,#1606))
REPRESENTATION_CONTEXT('','3D')
);
#1603=(
LENGTH_UNIT()
NAMED_UNIT(*)
SI_UNIT(.MILLI.,.METRE.)
);
#1605=(
NAMED_UNIT(*)
PLANE_ANGLE_UNIT()
SI_UNIT($,.RADIAN.)
);
#1606=(
NAMED_UNIT(*)
SI_UNIT($,.STERADIAN.)
SOLID_ANGLE_UNIT()
);
#1609=SHAPE_DEFINITION_REPRESENTATION(#1618,#1635);
#1618=PRODUCT_DEFINITION_SHAPE('',$,#1645);
#1635=SHAPE_REPRESENTATION('',(#911),#1595);
#1642=PRODUCT_DEFINITION_CONTEXT('part definition',#1671,'design');
#1645=PRODUCT_DEFINITION('Pin_03','Pin_03',#1654,#1642);
#1654=PRODUCT_DEFINITION_FORMATION('',$,#1675);
#1671=APPLICATION_CONTEXT(
'Core Data for Automotive Mechanical Design Process');
#1672=PRODUCT_CONTEXT('part definition',#1671,'mechanical');
#1675=PRODUCT('Pin_03','Pin_03',$,(#1672));
#1684=PRESENTATION_STYLE_ASSIGNMENT((#1688));
#1688=SURFACE_STYLE_USAGE(.BOTH.,#1692);
#1692=SURFACE_SIDE_STYLE('',(#1696));
#1696=SURFACE_STYLE_FILL_AREA(#1700);
#1700=FILL_AREA_STYLE('Opaque(160,160,160)',(#1704));
#1704=FILL_AREA_STYLE_COLOUR('Opaque(160,160,160)',#1708);
#1708=COLOUR_RGB('Opaque(160,160,160)', 0.66274510, 0.83137255, 0.94901961);
ENDSEC;
END-ISO-10303-21;
